ISO-10303-21;
HEADER;
FILE_DESCRIPTION (('STEP AP203'),
    '1' );
FILE_NAME ('Cleco, Fastener, Center, Split.step',
    '2026-10-09T13:45:32',
    ( '' ),
    ( '' ),
    'SwSTEP 2.0',
    'SolidWorks 2024',
    '' );
FILE_SCHEMA (( 'AUTOMOTIVE_DESIGN' ));
ENDSEC;

DATA;
#31=ORIENTED_EDGE ( 'NONE', *, *, #3836, .F. ) ;
#54=DIRECTION ( 'NONE',  ( -0.000000000000000000, -0.000000000000000000, -1.000000000000000000 ) ) ;
#68=EDGE_CURVE ( 'NONE', #5482, #3124, #1464, .T. ) ;
#113=DIRECTION ( 'NONE',  ( 0.000000000000000000, 0.000000000000000000, -1.000000000000000000 ) ) ;
#116=DIRECTION ( 'NONE',  ( 1.000000000000000000, -0.000000000000000000, -0.000000000000000000 ) ) ;
#135=DIRECTION ( 'NONE',  ( 1.000000000000000000, 0.000000000000000000, 0.000000000000000000 ) ) ;
#145=EDGE_LOOP ( 'NONE', ( #637, #5534, #4273, #3035, #377, #5498, #741, #1949, #1567, #4620 ) ) ;
#172=PRODUCT_DEFINITION ( 'UNKNOWN', '', #7483, #3514 ) ;
#209=ORIENTED_EDGE ( 'NONE', *, *, #2574, .T. ) ;
#221=DIRECTION ( 'NONE',  ( 0.000000000000000000, 1.000000000000000000, 0.000000000000000000 ) ) ;
#227=VECTOR ( 'NONE', #2539, 39.37007874015748143 ) ;
#240=ORIENTED_EDGE ( 'NONE', *, *, #562, .T. ) ;
#291=ORIENTED_EDGE ( 'NONE', *, *, #4442, .F. ) ;
#300=CARTESIAN_POINT ( 'NONE',  ( -0.09999999999999997780, 0.03125000000000000000, 0.7124999999999989120 ) ) ;
#309=ORIENTED_EDGE ( 'NONE', *, *, #5941, .T. ) ;
#316=ORIENTED_EDGE ( 'NONE', *, *, #3989, .T. ) ;
#363=CARTESIAN_POINT ( 'NONE',  ( 0.000000000000000000, 0.03125000000000000000, 0.2896281645421511231 ) ) ;
#376=EDGE_CURVE ( 'NONE', #6326, #5482, #5761, .T. ) ;
#377=ORIENTED_EDGE ( 'NONE', *, *, #5359, .T. ) ;
#391=CARTESIAN_POINT ( 'NONE',  ( 0.1000000000000000472, -0.03125000000000000000, 0.8125000000000000000 ) ) ;
#397=LINE ( 'NONE', #5407, #5717 ) ;
#400=CARTESIAN_POINT ( 'NONE',  ( -0.1249999999999999445, -0.03125000000000000000, 0.06250000000000000000 ) ) ;
#408=EDGE_LOOP ( 'NONE', ( #911, #4021, #6469, #4113 ) ) ;
#422=EDGE_LOOP ( 'NONE', ( #1983, #4838 ) ) ;
#427=DIRECTION ( 'NONE',  ( 0.000000000000000000, 0.000000000000000000, -1.000000000000000000 ) ) ;
#433=DIRECTION ( 'NONE',  ( -0.000000000000000000, -0.000000000000000000, -1.000000000000000000 ) ) ;
#436=CARTESIAN_POINT ( 'NONE',  ( -0.09999999999999997780, 0.03125000000000000000, 0.06250000000000000000 ) ) ;
#444=CARTESIAN_POINT ( 'NONE',  ( -0.09999999999999997780, -0.03125000000000000000, 0.8125000000000000000 ) ) ;
#453=DIRECTION ( 'NONE',  ( 0.000000000000000000, 0.000000000000000000, -1.000000000000000000 ) ) ;
#462=ORIENTED_EDGE ( 'NONE', *, *, #7249, .T. ) ;
#496=MECHANICAL_CONTEXT ( 'NONE', #2361, 'mechanical' ) ;
#558=LINE ( 'NONE', #2358, #607 ) ;
#560=VECTOR ( 'NONE', #1957, 39.37007874015748143 ) ;
#562=EDGE_CURVE ( 'NONE', #5236, #762, #5047, .T. ) ;
#569=CARTESIAN_POINT ( 'NONE',  ( 2.023273750469992349E-18, 0.03125000000000000000, 0.3061494484901324808 ) ) ;
#607=VECTOR ( 'NONE', #3065, 39.37007874015748143 ) ;
#622=ADVANCED_FACE ( 'NONE', ( #4895 ), #6816, .T. ) ;
#627=AXIS2_PLACEMENT_3D ( 'NONE', #3489, #7212, #920 ) ;
#637=ORIENTED_EDGE ( 'NONE', *, *, #6793, .F. ) ;
#645=ORIENTED_EDGE ( 'NONE', *, *, #7249, .F. ) ;
#693=DIRECTION ( 'NONE',  ( -1.000000000000000000, 0.000000000000000000, -0.000000000000000000 ) ) ;
#701=CARTESIAN_POINT ( 'NONE',  ( 0.000000000000000000, 0.03125000000000000000, 0.6646281645421511231 ) ) ;
#741=ORIENTED_EDGE ( 'NONE', *, *, #1281, .F. ) ;
#756=CARTESIAN_POINT ( 'NONE',  ( -0.06999999999999996503, -0.03125000000000000000, 0.8125000000000000000 ) ) ;
#762=VERTEX_POINT ( 'NONE', #1967 ) ;
#764=ORIENTED_EDGE ( 'NONE', *, *, #3989, .F. ) ;
#851=VECTOR ( 'NONE', #433, 39.37007874015748143 ) ;
#873=VERTEX_POINT ( 'NONE', #7144 ) ;
#877=PRODUCT_DEFINITION_SHAPE ( 'NONE', 'NONE',  #172 ) ;
#911=ORIENTED_EDGE ( 'NONE', *, *, #5030, .T. ) ;
#920=DIRECTION ( 'NONE',  ( 1.000000000000000000, 0.000000000000000000, -0.000000000000000000 ) ) ;
#940=LINE ( 'NONE', #7171, #1865 ) ;
#1004=VERTEX_POINT ( 'NONE', #4926 ) ;
#1032=DIRECTION ( 'NONE',  ( 0.000000000000000000, 1.000000000000000000, -0.000000000000000000 ) ) ;
#1033=SHAPE_DEFINITION_REPRESENTATION ( #877, #2774 ) ;
#1069=PLANE ( 'NONE',  #4488 ) ;
#1077=DIRECTION ( 'NONE',  ( 6.975840231036812635E-15, -1.000000000000000000, -2.013666839457971600E-30 ) ) ;
#1089=VECTOR ( 'NONE', #5990, 39.37007874015748143 ) ;
#1096=CARTESIAN_POINT ( 'NONE',  ( 0.1250000000000000278, -0.03125000000000000000, 0.06250000000000000000 ) ) ;
#1100=CIRCLE ( 'NONE', #1627, 0.01652128394798136474 ) ;
#1114=DIRECTION ( 'NONE',  ( 0.9578262852211522071, 0.000000000000000000, -0.2873478855663425535 ) ) ;
#1133=DIRECTION ( 'NONE',  ( 0.000000000000000000, 1.000000000000000000, 0.000000000000000000 ) ) ;
#1143=PLANE ( 'NONE',  #3737 ) ;
#1159=DIRECTION ( 'NONE',  ( 0.000000000000000000, 1.000000000000000000, 0.000000000000000000 ) ) ;
#1191=DIRECTION ( 'NONE',  ( 1.000000000000000000, -0.000000000000000000, -0.000000000000000000 ) ) ;
#1214=CARTESIAN_POINT ( 'NONE',  ( 0.07000000000000002054, -0.03125000000000000000, 0.8125000000000000000 ) ) ;
#1215=PLANE ( 'NONE',  #5588 ) ;
#1225=DIRECTION ( 'NONE',  ( 1.000000000000000000, 0.000000000000000000, 0.000000000000000000 ) ) ;
#1241=DIRECTION ( 'NONE',  ( -1.000000000000000000, -6.975840231036812635E-15, 0.000000000000000000 ) ) ;
#1244=ORIENTED_EDGE ( 'NONE', *, *, #1432, .T. ) ;
#1254=DIRECTION ( 'NONE',  ( 1.000000000000000000, 0.000000000000000000, 0.000000000000000000 ) ) ;
#1263=CARTESIAN_POINT ( 'NONE',  ( -0.09999999999999997780, -0.03125000000000000000, 0.8125000000000000000 ) ) ;
#1281=EDGE_CURVE ( 'NONE', #7143, #4391, #5292, .T. ) ;
#1296=ORIENTED_EDGE ( 'NONE', *, *, #5085, .F. ) ;
#1303=DIRECTION ( 'NONE',  ( 0.000000000000000000, -1.000000000000000000, 0.000000000000000000 ) ) ;
#1339=FACE_OUTER_BOUND ( 'NONE', #3134, .T. ) ;
#1340=LINE ( 'NONE', #3969, #5186 ) ;
#1344=DIRECTION ( 'NONE',  ( 0.000000000000000000, 0.000000000000000000, -1.000000000000000000 ) ) ;
#1349=DIRECTION ( 'NONE',  ( -1.000000000000000000, 0.000000000000000000, 0.000000000000000000 ) ) ;
#1356=ORIENTED_EDGE ( 'NONE', *, *, #5085, .T. ) ;
#1371=ORIENTED_EDGE ( 'NONE', *, *, #68, .T. ) ;
#1374=EDGE_CURVE ( 'NONE', #6326, #2455, #8050, .T. ) ;
#1432=EDGE_CURVE ( 'NONE', #3897, #7385, #558, .T. ) ;
#1446=ORIENTED_EDGE ( 'NONE', *, *, #5030, .F. ) ;
#1464=LINE ( 'NONE', #5210, #851 ) ;
#1484=ORIENTED_EDGE ( 'NONE', *, *, #6793, .T. ) ;
#1505=CIRCLE ( 'NONE', #7907, 0.01652128394798136474 ) ;
#1517=CARTESIAN_POINT ( 'NONE',  ( -0.1249999999999999445, -0.03125000000000000000, 0.06250000000000000000 ) ) ;
#1520=DIRECTION ( 'NONE',  ( 0.000000000000000000, 0.000000000000000000, 1.000000000000000000 ) ) ;
#1551=LINE ( 'NONE', #2976, #2532 ) ;
#1567=ORIENTED_EDGE ( 'NONE', *, *, #68, .F. ) ;
#1627=AXIS2_PLACEMENT_3D ( 'NONE', #7809, #4012, #4662 ) ;
#1645=VERTEX_POINT ( 'NONE', #2687 ) ;
#1651=SPHERICAL_SURFACE ( 'NONE', #2854, 0.01652128394798136474 ) ;
#1663=EDGE_LOOP ( 'NONE', ( #31, #2092, #1356, #4244 ) ) ;
#1664=DIRECTION ( 'NONE',  ( -0.000000000000000000, -1.000000000000000000, -0.000000000000000000 ) ) ;
#1681=CARTESIAN_POINT ( 'NONE',  ( 0.1250000000000000278, -0.03125000000000000000, 0.06250000000000000000 ) ) ;
#1701=DIRECTION ( 'NONE',  ( 0.000000000000000000, 1.000000000000000000, 0.000000000000000000 ) ) ;
#1772=LINE ( 'NONE', #2417, #5060 ) ;
#1773=EDGE_CURVE ( 'NONE', #2220, #6593, #940, .T. ) ;
#1789=ORIENTED_EDGE ( 'NONE', *, *, #376, .F. ) ;
#1806=FACE_OUTER_BOUND ( 'NONE', #5859, .T. ) ;
#1817=DIRECTION ( 'NONE',  ( 0.000000000000000000, 1.000000000000000000, -0.000000000000000000 ) ) ;
#1848=DIRECTION ( 'NONE',  ( -0.2873478855663425535, 0.000000000000000000, -0.9578262852211522071 ) ) ;
#1865=VECTOR ( 'NONE', #4057, 39.37007874015748143 ) ;
#1870=DIRECTION ( 'NONE',  ( -0.9578262852211522071, 0.000000000000000000, -0.2873478855663426645 ) ) ;
#1882=VECTOR ( 'NONE', #1664, 39.37007874015748143 ) ;
#1884=DIRECTION ( 'NONE',  ( -1.000000000000000000, 6.975840231036812635E-15, 0.000000000000000000 ) ) ;
#1889=CARTESIAN_POINT ( 'NONE',  ( -0.06999999999999996503, 0.03125000000000000000, 0.8125000000000000000 ) ) ;
#1943=VERTEX_POINT ( 'NONE', #2711 ) ;
#1949=ORIENTED_EDGE ( 'NONE', *, *, #4798, .F. ) ;
#1957=DIRECTION ( 'NONE',  ( -1.000000000000000000, 0.000000000000000000, 0.000000000000000000 ) ) ;
#1965=SPHERICAL_SURFACE ( 'NONE', #5454, 0.01652128394798136474 ) ;
#1967=CARTESIAN_POINT ( 'NONE',  ( 2.023273750469992349E-18, -0.03125000000000000000, 0.6481068805941697653 ) ) ;
#1983=ORIENTED_EDGE ( 'NONE', *, *, #3983, .F. ) ;
#1986=EDGE_LOOP ( 'NONE', ( #7378, #7954, #1484, #7990 ) ) ;
#2032=ORIENTED_EDGE ( 'NONE', *, *, #7149, .F. ) ;
#2042=ORIENTED_EDGE ( 'NONE', *, *, #5043, .F. ) ;
#2058=CARTESIAN_POINT ( 'NONE',  ( 0.000000000000000000, 0.03125000000000000000, 0.2896281645421511231 ) ) ;
#2086=ADVANCED_FACE ( 'NONE', ( #4849 ), #1069, .F. ) ;
#2087=CARTESIAN_POINT ( 'NONE',  ( 0.1250000000000000278, -0.03125000000000000000, 0.06250000000000000000 ) ) ;
#2092=ORIENTED_EDGE ( 'NONE', *, *, #4442, .T. ) ;
#2103=FACE_OUTER_BOUND ( 'NONE', #6381, .T. ) ;
#2122=( GEOMETRIC_REPRESENTATION_CONTEXT ( 3 ) GLOBAL_UNCERTAINTY_ASSIGNED_CONTEXT ( ( #8080 ) ) GLOBAL_UNIT_ASSIGNED_CONTEXT ( ( #7387, #4891, #7344 ) ) REPRESENTATION_CONTEXT ( 'NONE', 'WORKASPACE' ) );
#2127=DIRECTION ( 'NONE',  ( 0.000000000000000000, -1.000000000000000000, 0.000000000000000000 ) ) ;
#2131=LINE ( 'NONE', #1517, #5674 ) ;
#2148=VECTOR ( 'NONE', #3877, 39.37007874015748143 ) ;
#2153=ORIENTED_EDGE ( 'NONE', *, *, #2533, .F. ) ;
#2171=VECTOR ( 'NONE', #4664, 39.37007874015748143 ) ;
#2204=CARTESIAN_POINT ( 'NONE',  ( 0.000000000000000000, 0.03125000000000000000, 0.2896281645421511231 ) ) ;
#2205=LINE ( 'NONE', #391, #2171 ) ;
#2218=PLANE ( 'NONE',  #627 ) ;
#2220=VERTEX_POINT ( 'NONE', #3080 ) ;
#2233=ORIENTED_EDGE ( 'NONE', *, *, #7079, .F. ) ;
#2285=ADVANCED_FACE ( 'NONE', ( #3244 ), #7014, .T. ) ;
#2290=CLOSED_SHELL ( 'NONE', ( #5596, #3139, #6249, #4803, #4357, #2285, #5797, #3926, #4482, #2785, #4790, #2086, #622, #4490, #7641, #5384 ) ) ;
#2291=AXIS2_PLACEMENT_3D ( 'NONE', #4433, #6238, #1884 ) ;
#2292=CARTESIAN_POINT ( 'NONE',  ( 0.1000000000000000472, 0.03125000000000000000, 0.06250000000000000000 ) ) ;
#2336=FACE_BOUND ( 'NONE', #7313, .T. ) ;
#2358=CARTESIAN_POINT ( 'NONE',  ( 0.1250000000000000278, -0.03125000000000000000, 0.000000000000000000 ) ) ;
#2361=APPLICATION_CONTEXT ( 'configuration controlled 3d designs of mechanical parts and assemblies' ) ;
#2378=EDGE_LOOP ( 'NONE', ( #645, #2233 ) ) ;
#2417=CARTESIAN_POINT ( 'NONE',  ( 0.1000000000000000472, -0.03125000000000000000, 0.06250000000000000000 ) ) ;
#2455=VERTEX_POINT ( 'NONE', #4756 ) ;
#2461=ORIENTED_EDGE ( 'NONE', *, *, #1281, .T. ) ;
#2481=CARTESIAN_POINT ( 'NONE',  ( 0.1250000000000000278, 0.03125000000000000000, 0.06250000000000000000 ) ) ;
#2489=FACE_OUTER_BOUND ( 'NONE', #6202, .T. ) ;
#2492=LINE ( 'NONE', #5000, #7173 ) ;
#2504=ORIENTED_EDGE ( 'NONE', *, *, #6683, .F. ) ;
#2532=VECTOR ( 'NONE', #3467, 39.37007874015748143 ) ;
#2533=EDGE_CURVE ( 'NONE', #7143, #6082, #3484, .T. ) ;
#2539=DIRECTION ( 'NONE',  ( 0.2873478855663425535, -0.000000000000000000, 0.9578262852211522071 ) ) ;
#2543=CIRCLE ( 'NONE', #7128, 0.01652128394798136474 ) ;
#2553=ORIENTED_EDGE ( 'NONE', *, *, #3088, .T. ) ;
#2566=FACE_OUTER_BOUND ( 'NONE', #3952, .T. ) ;
#2569=ORIENTED_EDGE ( 'NONE', *, *, #5838, .T. ) ;
#2574=EDGE_CURVE ( 'NONE', #6082, #3897, #2131, .T. ) ;
#2582=CIRCLE ( 'NONE', #7036, 0.01652128394798136474 ) ;
#2649=LINE ( 'NONE', #2087, #4801 ) ;
#2684=VERTEX_POINT ( 'NONE', #5573 ) ;
#2687=CARTESIAN_POINT ( 'NONE',  ( 0.1250000000000000278, 0.03125000000000000000, 0.000000000000000000 ) ) ;
#2711=CARTESIAN_POINT ( 'NONE',  ( 0.1000000000000000472, -0.03125000000000000000, 0.7124999999999989120 ) ) ;
#2759=VERTEX_POINT ( 'NONE', #6278 ) ;
#2774=SHAPE_REPRESENTATION ( 'Cleco, Fastener, Center, Split', ( #3555 ), #2122 ) ;
#2778=DIRECTION ( 'NONE',  ( 0.000000000000000000, 0.000000000000000000, -1.000000000000000000 ) ) ;
#2785=ADVANCED_FACE ( 'NONE', ( #7045 ), #5695, .F. ) ;
#2801=EDGE_CURVE ( 'NONE', #1645, #4391, #6312, .T. ) ;
#2854=AXIS2_PLACEMENT_3D ( 'NONE', #7270, #7834, #5924 ) ;
#2860=ORIENTED_EDGE ( 'NONE', *, *, #376, .T. ) ;
#2892=EDGE_LOOP ( 'NONE', ( #462, #4178 ) ) ;
#2894=FACE_OUTER_BOUND ( 'NONE', #408, .T. ) ;
#2927=VECTOR ( 'NONE', #6631, 39.37007874015748143 ) ;
#2928=CARTESIAN_POINT ( 'NONE',  ( 0.1000000000000000472, -0.03125000000000000000, 0.8125000000000000000 ) ) ;
#2937=AXIS2_PLACEMENT_3D ( 'NONE', #2928, #7318, #4778 ) ;
#2976=CARTESIAN_POINT ( 'NONE',  ( 0.07000000000000002054, -0.03125000000000000000, 0.8125000000000000000 ) ) ;
#2996=CARTESIAN_POINT ( 'NONE',  ( -0.1249999999999999445, 0.03125000000000000000, 0.000000000000000000 ) ) ;
#3035=ORIENTED_EDGE ( 'NONE', *, *, #7687, .F. ) ;
#3040=EDGE_CURVE ( 'NONE', #4391, #3897, #7730, .T. ) ;
#3065=DIRECTION ( 'NONE',  ( 1.000000000000000000, -0.000000000000000000, -0.000000000000000000 ) ) ;
#3066=EDGE_LOOP ( 'NONE', ( #6690, #6809, #2153, #2461 ) ) ;
#3072=LINE ( 'NONE', #3732, #4815 ) ;
#3080=CARTESIAN_POINT ( 'NONE',  ( -0.06999999999999996503, -0.03125000000000000000, 0.8125000000000000000 ) ) ;
#3088=EDGE_CURVE ( 'NONE', #3124, #2455, #3520, .T. ) ;
#3097=CARTESIAN_POINT ( 'NONE',  ( 0.000000000000000000, -0.03125000000000000000, 0.3061494484901324808 ) ) ;
#3124=VERTEX_POINT ( 'NONE', #436 ) ;
#3134=EDGE_LOOP ( 'NONE', ( #7282, #2860, #1371, #2553 ) ) ;
#3139=ADVANCED_FACE ( 'NONE', ( #2894 ), #5400, .F. ) ;
#3155=DIRECTION ( 'NONE',  ( 0.000000000000000000, 0.000000000000000000, -1.000000000000000000 ) ) ;
#3214=AXIS2_PLACEMENT_3D ( 'NONE', #6132, #1077, #1241 ) ;
#3244=FACE_OUTER_BOUND ( 'NONE', #7407, .T. ) ;
#3320=ORIENTED_EDGE ( 'NONE', *, *, #4798, .T. ) ;
#3321=DIRECTION ( 'NONE',  ( 0.000000000000000000, -0.000000000000000000, 1.000000000000000000 ) ) ;
#3354=ORIENTED_EDGE ( 'NONE', *, *, #2801, .F. ) ;
#3467=DIRECTION ( 'NONE',  ( -0.2873478855663426645, -0.000000000000000000, 0.9578262852211522071 ) ) ;
#3470=VECTOR ( 'NONE', #1303, 39.37007874015748143 ) ;
#3484=LINE ( 'NONE', #400, #1089 ) ;
#3489=CARTESIAN_POINT ( 'NONE',  ( 0.1250000000000000278, 0.03125000000000000000, 0.06250000000000000000 ) ) ;
#3513=CARTESIAN_POINT ( 'NONE',  ( -0.1249999999999999445, -0.03125000000000000000, 0.000000000000000000 ) ) ;
#3514=DESIGN_CONTEXT ( 'detailed design', #7559, 'design' ) ;
#3520=LINE ( 'NONE', #5481, #1882 ) ;
#3526=FACE_BOUND ( 'NONE', #5617, .T. ) ;
#3547=ORIENTED_EDGE ( 'NONE', *, *, #3983, .T. ) ;
#3555=AXIS2_PLACEMENT_3D ( 'NONE', #5720, #6981, #135 ) ;
#3563=CARTESIAN_POINT ( 'NONE',  ( 0.000000000000000000, -0.03125000000000000000, 0.2896281645421511231 ) ) ;
#3568=DIRECTION ( 'NONE',  ( 0.000000000000000000, -1.000000000000000000, 0.000000000000000000 ) ) ;
#3594=ORIENTED_EDGE ( 'NONE', *, *, #4388, .T. ) ;
#3607=ORIENTED_EDGE ( 'NONE', *, *, #5350, .F. ) ;
#3612=DIRECTION ( 'NONE',  ( 0.000000000000000000, 0.000000000000000000, 1.000000000000000000 ) ) ;
#3623=ORIENTED_EDGE ( 'NONE', *, *, #562, .F. ) ;
#3625=VECTOR ( 'NONE', #1349, 39.37007874015748143 ) ;
#3663=VERTEX_POINT ( 'NONE', #3906 ) ;
#3710=ORIENTED_EDGE ( 'NONE', *, *, #3088, .F. ) ;
#3732=CARTESIAN_POINT ( 'NONE',  ( -0.06999999999999996503, -0.03125000000000000000, 0.8125000000000000000 ) ) ;
#3737=AXIS2_PLACEMENT_3D ( 'NONE', #1214, #1870, #3806 ) ;
#3751=CIRCLE ( 'NONE', #4669, 0.01652128394798136474 ) ;
#3760=MANIFOLD_SOLID_BREP ( 'LPattern1', #2290 ) ;
#3769=DIRECTION ( 'NONE',  ( 0.000000000000000000, 0.000000000000000000, -1.000000000000000000 ) ) ;
#3780=CARTESIAN_POINT ( 'NONE',  ( -0.1249999999999999445, 0.03125000000000000000, 0.06250000000000000000 ) ) ;
#3796=EDGE_LOOP ( 'NONE', ( #3710, #3320, #6287, #309 ) ) ;
#3806=DIRECTION ( 'NONE',  ( -0.2873478855663426645, 0.000000000000000000, 0.9578262852211522071 ) ) ;
#3836=EDGE_CURVE ( 'NONE', #7370, #4400, #5103, .T. ) ;
#3853=ADVANCED_BREP_SHAPE_REPRESENTATION ( '', ( #3760, #3555 ), #2122 ) ;
#3857=CARTESIAN_POINT ( 'NONE',  ( 0.1000000000000000472, 0.03125000000000000000, 0.7124999999999989120 ) ) ;
#3862=LINE ( 'NONE', #7057, #3625 ) ;
#3877=DIRECTION ( 'NONE',  ( -0.000000000000000000, -0.000000000000000000, -1.000000000000000000 ) ) ;
#3897=VERTEX_POINT ( 'NONE', #3513 ) ;
#3906=CARTESIAN_POINT ( 'NONE',  ( 0.1000000000000000472, -0.03125000000000000000, 0.06250000000000000000 ) ) ;
#3913=CARTESIAN_POINT ( 'NONE',  ( 0.1000000000000000472, 0.03125000000000000000, 0.8125000000000000000 ) ) ;
#3926=ADVANCED_FACE ( 'NONE', ( #5971 ), #7199, .F. ) ;
#3952=EDGE_LOOP ( 'NONE', ( #2042, #291, #6339, #2504 ) ) ;
#3969=CARTESIAN_POINT ( 'NONE',  ( 0.1250000000000000278, -0.03125000000000000000, 0.06250000000000000000 ) ) ;
#3983=EDGE_CURVE ( 'NONE', #4234, #7191, #2543, .T. ) ;
#3989=EDGE_CURVE ( 'NONE', #4051, #1004, #1100, .T. ) ;
#3994=AXIS2_PLACEMENT_3D ( 'NONE', #1681, #4713, #4842 ) ;
#4002=CARTESIAN_POINT ( 'NONE',  ( 0.000000000000000000, 0.03125000000000000000, 0.6646281645421511231 ) ) ;
#4012=DIRECTION ( 'NONE',  ( 0.000000000000000000, 1.000000000000000000, -0.000000000000000000 ) ) ;
#4020=VECTOR ( 'NONE', #5255, 39.37007874015748143 ) ;
#4021=ORIENTED_EDGE ( 'NONE', *, *, #5359, .F. ) ;
#4051=VERTEX_POINT ( 'NONE', #3097 ) ;
#4057=DIRECTION ( 'NONE',  ( 1.000000000000000000, -0.000000000000000000, -0.000000000000000000 ) ) ;
#4063=ORIENTED_EDGE ( 'NONE', *, *, #7583, .F. ) ;
#4112=VECTOR ( 'NONE', #1701, 39.37007874015748143 ) ;
#4113=ORIENTED_EDGE ( 'NONE', *, *, #8079, .T. ) ;
#4137=DIRECTION ( 'NONE',  ( -0.000000000000000000, -0.000000000000000000, -1.000000000000000000 ) ) ;
#4157=ORIENTED_EDGE ( 'NONE', *, *, #1773, .F. ) ;
#4176=DIRECTION ( 'NONE',  ( 0.000000000000000000, -1.000000000000000000, 0.000000000000000000 ) ) ;
#4178=ORIENTED_EDGE ( 'NONE', *, *, #7079, .T. ) ;
#4209=LINE ( 'NONE', #6750, #5068 ) ;
#4234=VERTEX_POINT ( 'NONE', #4559 ) ;
#4241=AXIS2_PLACEMENT_3D ( 'NONE', #1096, #6710, #7325 ) ;
#4242=ORIENTED_EDGE ( 'NONE', *, *, #1374, .T. ) ;
#4244=ORIENTED_EDGE ( 'NONE', *, *, #7583, .T. ) ;
#4273=ORIENTED_EDGE ( 'NONE', *, *, #3836, .T. ) ;
#4304=VERTEX_POINT ( 'NONE', #5299 ) ;
#4307=CARTESIAN_POINT ( 'NONE',  ( 0.1250000000000000278, 0.03125000000000000000, 0.000000000000000000 ) ) ;
#4357=ADVANCED_FACE ( 'NONE', ( #2336, #3526, #6027 ), #6157, .F. ) ;
#4363=DIRECTION ( 'NONE',  ( 0.000000000000000000, 0.000000000000000000, 1.000000000000000000 ) ) ;
#4379=CARTESIAN_POINT ( 'NONE',  ( -0.1249999999999999445, -0.03125000000000000000, 0.06250000000000000000 ) ) ;
#4388=EDGE_CURVE ( 'NONE', #1004, #4051, #1505, .T. ) ;
#4391=VERTEX_POINT ( 'NONE', #2996 ) ;
#4399=AXIS2_PLACEMENT_3D ( 'NONE', #1263, #1225, #3155 ) ;
#4400=VERTEX_POINT ( 'NONE', #2292 ) ;
#4424=AXIS2_PLACEMENT_3D ( 'NONE', #4002, #3568, #453 ) ;
#4428=CARTESIAN_POINT ( 'NONE',  ( -0.09999999999999997780, -0.03125000000000000000, 0.7124999999999989120 ) ) ;
#4433=CARTESIAN_POINT ( 'NONE',  ( 0.000000000000000000, -0.03125000000000000000, 0.6646281645421511231 ) ) ;
#4442=EDGE_CURVE ( 'NONE', #7370, #1943, #5341, .T. ) ;
#4471=DIRECTION ( 'NONE',  ( 6.975840231036812635E-15, -1.000000000000000000, -2.013666839457971600E-30 ) ) ;
#4475=VECTOR ( 'NONE', #54, 39.37007874015748143 ) ;
#4482=ADVANCED_FACE ( 'NONE', ( #1339 ), #7538, .F. ) ;
#4488=AXIS2_PLACEMENT_3D ( 'NONE', #6076, #1114, #1848 ) ;
#4490=ADVANCED_FACE ( 'NONE', ( #1806 ), #4962, .T. ) ;
#4500=CARTESIAN_POINT ( 'NONE',  ( -0.09999999999999997780, -0.03125000000000000000, 0.8125000000000000000 ) ) ;
#4524=LINE ( 'NONE', #7026, #7298 ) ;
#4538=CARTESIAN_POINT ( 'NONE',  ( 0.1000000000000000472, 0.03125000000000000000, 0.8125000000000000000 ) ) ;
#4554=AXIS2_PLACEMENT_3D ( 'NONE', #701, #2127, #1344 ) ;
#4559=CARTESIAN_POINT ( 'NONE',  ( 0.000000000000000000, 0.03125000000000000000, 0.2731068805941697653 ) ) ;
#4620=ORIENTED_EDGE ( 'NONE', *, *, #7234, .T. ) ;
#4621=CARTESIAN_POINT ( 'NONE',  ( -0.1249999999999999445, -0.03125000000000000000, 0.000000000000000000 ) ) ;
#4662=DIRECTION ( 'NONE',  ( 0.000000000000000000, 0.000000000000000000, 1.000000000000000000 ) ) ;
#4664=DIRECTION ( 'NONE',  ( -0.000000000000000000, -0.000000000000000000, -1.000000000000000000 ) ) ;
#4669=AXIS2_PLACEMENT_3D ( 'NONE', #363, #4176, #2778 ) ;
#4713=DIRECTION ( 'NONE',  ( 0.000000000000000000, 1.000000000000000000, -0.000000000000000000 ) ) ;
#4756=CARTESIAN_POINT ( 'NONE',  ( -0.09999999999999997780, -0.03125000000000000000, 0.06250000000000000000 ) ) ;
#4778=DIRECTION ( 'NONE',  ( 0.000000000000000000, 0.000000000000000000, 1.000000000000000000 ) ) ;
#4790=ADVANCED_FACE ( 'NONE', ( #2566 ), #1143, .F. ) ;
#4798=EDGE_CURVE ( 'NONE', #3124, #7143, #5614, .T. ) ;
#4801=VECTOR ( 'NONE', #116, 39.37007874015748143 ) ;
#4803=ADVANCED_FACE ( 'NONE', ( #8010 ), #7486, .F. ) ;
#4815=VECTOR ( 'NONE', #6803, 39.37007874015748143 ) ;
#4838=ORIENTED_EDGE ( 'NONE', *, *, #6093, .F. ) ;
#4842=DIRECTION ( 'NONE',  ( 0.000000000000000000, 0.000000000000000000, 1.000000000000000000 ) ) ;
#4849=FACE_OUTER_BOUND ( 'NONE', #5898, .T. ) ;
#4871=CARTESIAN_POINT ( 'NONE',  ( 0.1250000000000000278, 0.03125000000000000000, 0.06250000000000000000 ) ) ;
#4889=ORIENTED_EDGE ( 'NONE', *, *, #5941, .F. ) ;
#4891=( NAMED_UNIT ( * ) PLANE_ANGLE_UNIT ( ) SI_UNIT ( $, .RADIAN. ) );
#4895=FACE_OUTER_BOUND ( 'NONE', #2378, .T. ) ;
#4926=CARTESIAN_POINT ( 'NONE',  ( 2.023273750469992349E-18, -0.03125000000000000000, 0.2731068805941697653 ) ) ;
#4951=DIMENSIONAL_EXPONENTS ( 1.000000000000000000, 0.000000000000000000, 0.000000000000000000, 0.000000000000000000, 0.000000000000000000, 0.000000000000000000, 0.000000000000000000 ) ;
#4962=SPHERICAL_SURFACE ( 'NONE', #2291, 0.01652128394798136474 ) ;
#4987=FACE_BOUND ( 'NONE', #2892, .T. ) ;
#4993=CARTESIAN_POINT ( 'NONE',  ( 0.1250000000000000278, 0.03125000000000000000, 0.000000000000000000 ) ) ;
#4995=ORIENTED_EDGE ( 'NONE', *, *, #7234, .F. ) ;
#5000=CARTESIAN_POINT ( 'NONE',  ( 0.1250000000000000278, -0.03125000000000000000, 0.06250000000000000000 ) ) ;
#5030=EDGE_CURVE ( 'NONE', #7385, #1645, #5323, .T. ) ;
#5043=EDGE_CURVE ( 'NONE', #1943, #6593, #1551, .T. ) ;
#5047=CIRCLE ( 'NONE', #6358, 0.01652128394798136474 ) ;
#5060=VECTOR ( 'NONE', #1159, 39.37007874015748143 ) ;
#5068=VECTOR ( 'NONE', #1133, 39.37007874015748143 ) ;
#5085=EDGE_CURVE ( 'NONE', #1943, #3663, #2205, .T. ) ;
#5103=LINE ( 'NONE', #4538, #2148 ) ;
#5137=AXIS2_PLACEMENT_3D ( 'NONE', #7582, #3321, #5821 ) ;
#5138=ORIENTED_EDGE ( 'NONE', *, *, #8079, .F. ) ;
#5186=VECTOR ( 'NONE', #6926, 39.37007874015748143 ) ;
#5210=CARTESIAN_POINT ( 'NONE',  ( -0.09999999999999997780, 0.03125000000000000000, 0.8125000000000000000 ) ) ;
#5236=VERTEX_POINT ( 'NONE', #6221 ) ;
#5255=DIRECTION ( 'NONE',  ( -0.000000000000000000, -0.000000000000000000, -1.000000000000000000 ) ) ;
#5292=LINE ( 'NONE', #5868, #4020 ) ;
#5294=DIRECTION ( 'NONE',  ( -0.000000000000000000, -0.000000000000000000, -1.000000000000000000 ) ) ;
#5299=CARTESIAN_POINT ( 'NONE',  ( 0.000000000000000000, 0.03125000000000000000, 0.6481068805941697653 ) ) ;
#5323=LINE ( 'NONE', #7846, #4112 ) ;
#5341=LINE ( 'NONE', #6280, #3470 ) ;
#5350=EDGE_CURVE ( 'NONE', #7484, #2220, #6369, .T. ) ;
#5359=EDGE_CURVE ( 'NONE', #2759, #1645, #4524, .T. ) ;
#5384=ADVANCED_FACE ( 'NONE', ( #2103 ), #1651, .T. ) ;
#5400=PLANE ( 'NONE',  #4241 ) ;
#5407=CARTESIAN_POINT ( 'NONE',  ( 0.07000000000000002054, 0.03125000000000000000, 0.8125000000000000000 ) ) ;
#5454=AXIS2_PLACEMENT_3D ( 'NONE', #2058, #4471, #6974 ) ;
#5466=AXIS2_PLACEMENT_3D ( 'NONE', #4307, #8017, #7421 ) ;
#5481=CARTESIAN_POINT ( 'NONE',  ( -0.09999999999999997780, -0.03125000000000000000, 0.06250000000000000000 ) ) ;
#5482=VERTEX_POINT ( 'NONE', #300 ) ;
#5498=ORIENTED_EDGE ( 'NONE', *, *, #2801, .T. ) ;
#5534=ORIENTED_EDGE ( 'NONE', *, *, #6191, .T. ) ;
#5545=LENGTH_MEASURE_WITH_UNIT ( LENGTH_MEASURE( 0.02539999999999999897 ), #6081 );
#5573=CARTESIAN_POINT ( 'NONE',  ( 0.07000000000000002054, 0.03125000000000000000, 0.8125000000000000000 ) ) ;
#5588=AXIS2_PLACEMENT_3D ( 'NONE', #4871, #8049, #6063 ) ;
#5596=ADVANCED_FACE ( 'NONE', ( #7823 ), #2218, .T. ) ;
#5614=LINE ( 'NONE', #2481, #6468 ) ;
#5617=EDGE_LOOP ( 'NONE', ( #240, #8037 ) ) ;
#5624=LINE ( 'NONE', #1889, #227 ) ;
#5626=ORIENTED_EDGE ( 'NONE', *, *, #5043, .T. ) ;
#5634=EDGE_CURVE ( 'NONE', #762, #5236, #2582, .T. ) ;
#5674=VECTOR ( 'NONE', #5294, 39.37007874015748143 ) ;
#5695=PLANE ( 'NONE',  #6591 ) ;
#5696=EDGE_CURVE ( 'NONE', #2220, #6326, #3072, .T. ) ;
#5717=VECTOR ( 'NONE', #7890, 39.37007874015748143 ) ;
#5720=CARTESIAN_POINT ( 'NONE',  ( 0.000000000000000000, 0.000000000000000000, 0.000000000000000000 ) ) ;
#5757=CARTESIAN_POINT ( 'NONE',  ( 0.1250000000000000278, -0.03125000000000000000, 0.06250000000000000000 ) ) ;
#5758=DIRECTION ( 'NONE',  ( 0.000000000000000000, -1.000000000000000000, 0.000000000000000000 ) ) ;
#5761=LINE ( 'NONE', #7067, #7913 ) ;
#5797=ADVANCED_FACE ( 'NONE', ( #2489 ), #6767, .F. ) ;
#5821=DIRECTION ( 'NONE',  ( 1.000000000000000000, 0.000000000000000000, -0.000000000000000000 ) ) ;
#5838=EDGE_CURVE ( 'NONE', #5927, #2759, #1340, .T. ) ;
#5853=EDGE_LOOP ( 'NONE', ( #1296, #5626, #4157, #6160, #4242, #4889, #209, #1244, #5138, #2032 ) ) ;
#5859=EDGE_LOOP ( 'NONE', ( #3623, #6378 ) ) ;
#5868=CARTESIAN_POINT ( 'NONE',  ( -0.1249999999999999445, 0.03125000000000000000, 0.06250000000000000000 ) ) ;
#5869=ORIENTED_EDGE ( 'NONE', *, *, #1432, .F. ) ;
#5898=EDGE_LOOP ( 'NONE', ( #4995, #1789, #6006, #3607 ) ) ;
#5924=DIRECTION ( 'NONE',  ( -1.000000000000000000, 6.975840231036812635E-15, 0.000000000000000000 ) ) ;
#5927=VERTEX_POINT ( 'NONE', #7705 ) ;
#5941=EDGE_CURVE ( 'NONE', #6082, #2455, #2649, .T. ) ;
#5971=FACE_OUTER_BOUND ( 'NONE', #1663, .T. ) ;
#5986=CARTESIAN_POINT ( 'NONE',  ( -0.1249999999999999445, -0.03125000000000000000, 0.06250000000000000000 ) ) ;
#5989=CIRCLE ( 'NONE', #4424, 0.01652128394798136474 ) ;
#5990=DIRECTION ( 'NONE',  ( -0.000000000000000000, -1.000000000000000000, -0.000000000000000000 ) ) ;
#6006=ORIENTED_EDGE ( 'NONE', *, *, #5696, .F. ) ;
#6027=FACE_OUTER_BOUND ( 'NONE', #5853, .T. ) ;
#6063=DIRECTION ( 'NONE',  ( 0.000000000000000000, -0.000000000000000000, -1.000000000000000000 ) ) ;
#6076=CARTESIAN_POINT ( 'NONE',  ( -0.06999999999999996503, -0.03125000000000000000, 0.8125000000000000000 ) ) ;
#6081=( LENGTH_UNIT ( ) NAMED_UNIT ( * ) SI_UNIT ( $, .METRE. ) );
#6082=VERTEX_POINT ( 'NONE', #5986 ) ;
#6093=EDGE_CURVE ( 'NONE', #7191, #4234, #3751, .T. ) ;
#6132=CARTESIAN_POINT ( 'NONE',  ( 0.000000000000000000, 0.03125000000000000000, 0.6646281645421511231 ) ) ;
#6157=PLANE ( 'NONE',  #3994 ) ;
#6160=ORIENTED_EDGE ( 'NONE', *, *, #5696, .T. ) ;
#6191=EDGE_CURVE ( 'NONE', #2684, #7370, #397, .T. ) ;
#6202=EDGE_LOOP ( 'NONE', ( #1446, #5869, #7748, #3354 ) ) ;
#6221=CARTESIAN_POINT ( 'NONE',  ( 0.000000000000000000, -0.03125000000000000000, 0.6811494484901324808 ) ) ;
#6238=DIRECTION ( 'NONE',  ( -6.975840231036812635E-15, -1.000000000000000000, 2.013666839457971600E-30 ) ) ;
#6249=ADVANCED_FACE ( 'NONE', ( #7454, #4987, #7936 ), #1215, .F. ) ;
#6265=CIRCLE ( 'NONE', #4554, 0.01652128394798136474 ) ;
#6278=CARTESIAN_POINT ( 'NONE',  ( 0.1250000000000000278, 0.03125000000000000000, 0.06250000000000000000 ) ) ;
#6280=CARTESIAN_POINT ( 'NONE',  ( 0.1000000000000000472, -0.03125000000000000000, 0.7124999999999989120 ) ) ;
#6287=ORIENTED_EDGE ( 'NONE', *, *, #2533, .T. ) ;
#6289=CARTESIAN_POINT ( 'NONE',  ( -0.06999999999999996503, 0.03125000000000000000, 0.8125000000000000000 ) ) ;
#6312=LINE ( 'NONE', #4993, #560 ) ;
#6326=VERTEX_POINT ( 'NONE', #4428 ) ;
#6339=ORIENTED_EDGE ( 'NONE', *, *, #6191, .F. ) ;
#6358=AXIS2_PLACEMENT_3D ( 'NONE', #7391, #1817, #4363 ) ;
#6369=LINE ( 'NONE', #756, #6776 ) ;
#6371=DIRECTION ( 'NONE',  ( -1.000000000000000000, 0.000000000000000000, 0.000000000000000000 ) ) ;
#6378=ORIENTED_EDGE ( 'NONE', *, *, #5634, .F. ) ;
#6381=EDGE_LOOP ( 'NONE', ( #764, #7967 ) ) ;
#6411=DIRECTION ( 'NONE',  ( -0.000000000000000000, -0.000000000000000000, -1.000000000000000000 ) ) ;
#6449=LINE ( 'NONE', #5757, #4475 ) ;
#6468=VECTOR ( 'NONE', #6874, 39.37007874015748143 ) ;
#6469=ORIENTED_EDGE ( 'NONE', *, *, #5838, .F. ) ;
#6583=DIRECTION ( 'NONE',  ( 0.000000000000000000, -1.000000000000000000, 0.000000000000000000 ) ) ;
#6586=CARTESIAN_POINT ( 'NONE',  ( 0.07000000000000002054, -0.03125000000000000000, 0.8125000000000000000 ) ) ;
#6591=AXIS2_PLACEMENT_3D ( 'NONE', #4500, #113, #693 ) ;
#6593=VERTEX_POINT ( 'NONE', #6586 ) ;
#6631=DIRECTION ( 'NONE',  ( -0.000000000000000000, -1.000000000000000000, -0.000000000000000000 ) ) ;
#6632=VECTOR ( 'NONE', #4137, 39.37007874015748143 ) ;
#6639=VECTOR ( 'NONE', #6371, 39.37007874015748143 ) ;
#6683=EDGE_CURVE ( 'NONE', #6593, #2684, #4209, .T. ) ;
#6690=ORIENTED_EDGE ( 'NONE', *, *, #3040, .T. ) ;
#6710=DIRECTION ( 'NONE',  ( -1.000000000000000000, 0.000000000000000000, 0.000000000000000000 ) ) ;
#6750=CARTESIAN_POINT ( 'NONE',  ( 0.07000000000000002054, -0.03125000000000000000, 0.8125000000000000000 ) ) ;
#6752=AXIS2_PLACEMENT_3D ( 'NONE', #4379, #1254, #3769 ) ;
#6767=PLANE ( 'NONE',  #5466 ) ;
#6776=VECTOR ( 'NONE', #5758, 39.37007874015748143 ) ;
#6793=EDGE_CURVE ( 'NONE', #2684, #7484, #7028, .T. ) ;
#6803=DIRECTION ( 'NONE',  ( -0.2873478855663425535, -0.000000000000000000, -0.9578262852211522071 ) ) ;
#6809=ORIENTED_EDGE ( 'NONE', *, *, #2574, .F. ) ;
#6816=SPHERICAL_SURFACE ( 'NONE', #3214, 0.01652128394798136474 ) ;
#6874=DIRECTION ( 'NONE',  ( -1.000000000000000000, 0.000000000000000000, 0.000000000000000000 ) ) ;
#6880=ORIENTED_EDGE ( 'NONE', *, *, #7687, .T. ) ;
#6926=DIRECTION ( 'NONE',  ( 0.000000000000000000, 1.000000000000000000, 0.000000000000000000 ) ) ;
#6974=DIRECTION ( 'NONE',  ( -1.000000000000000000, -6.975840231036812635E-15, 0.000000000000000000 ) ) ;
#6981=DIRECTION ( 'NONE',  ( 0.000000000000000000, 0.000000000000000000, 1.000000000000000000 ) ) ;
#7014=PLANE ( 'NONE',  #5137 ) ;
#7026=CARTESIAN_POINT ( 'NONE',  ( 0.1250000000000000278, 0.03125000000000000000, 0.06250000000000000000 ) ) ;
#7028=LINE ( 'NONE', #3913, #6639 ) ;
#7036=AXIS2_PLACEMENT_3D ( 'NONE', #7138, #1032, #1520 ) ;
#7045=FACE_OUTER_BOUND ( 'NONE', #1986, .T. ) ;
#7057=CARTESIAN_POINT ( 'NONE',  ( 0.1250000000000000278, 0.03125000000000000000, 0.06250000000000000000 ) ) ;
#7067=CARTESIAN_POINT ( 'NONE',  ( -0.09999999999999997780, -0.03125000000000000000, 0.7124999999999989120 ) ) ;
#7079=EDGE_CURVE ( 'NONE', #873, #4304, #5989, .T. ) ;
#7128=AXIS2_PLACEMENT_3D ( 'NONE', #2204, #6583, #427 ) ;
#7138=CARTESIAN_POINT ( 'NONE',  ( 0.000000000000000000, -0.03125000000000000000, 0.6646281645421511231 ) ) ;
#7143=VERTEX_POINT ( 'NONE', #3780 ) ;
#7144=CARTESIAN_POINT ( 'NONE',  ( 2.023273750469992349E-18, 0.03125000000000000000, 0.6811494484901324808 ) ) ;
#7149=EDGE_CURVE ( 'NONE', #3663, #5927, #2492, .T. ) ;
#7171=CARTESIAN_POINT ( 'NONE',  ( 0.1000000000000000472, -0.03125000000000000000, 0.8125000000000000000 ) ) ;
#7173=VECTOR ( 'NONE', #1191, 39.37007874015748143 ) ;
#7178=EDGE_LOOP ( 'NONE', ( #3547, #7839 ) ) ;
#7191=VERTEX_POINT ( 'NONE', #569 ) ;
#7199=PLANE ( 'NONE',  #2937 ) ;
#7211=DIRECTION ( 'NONE',  ( 0.000000000000000000, 1.000000000000000000, -0.000000000000000000 ) ) ;
#7212=DIRECTION ( 'NONE',  ( 0.000000000000000000, -0.000000000000000000, 1.000000000000000000 ) ) ;
#7234=EDGE_CURVE ( 'NONE', #5482, #7484, #5624, .T. ) ;
#7249=EDGE_CURVE ( 'NONE', #4304, #873, #6265, .T. ) ;
#7270=CARTESIAN_POINT ( 'NONE',  ( 0.000000000000000000, -0.03125000000000000000, 0.2896281645421511231 ) ) ;
#7282=ORIENTED_EDGE ( 'NONE', *, *, #1374, .F. ) ;
#7298=VECTOR ( 'NONE', #6411, 39.37007874015748143 ) ;
#7310=ORIENTED_EDGE ( 'NONE', *, *, #7149, .T. ) ;
#7313=EDGE_LOOP ( 'NONE', ( #316, #3594 ) ) ;
#7318=DIRECTION ( 'NONE',  ( -1.000000000000000000, 0.000000000000000000, 0.000000000000000000 ) ) ;
#7325=DIRECTION ( 'NONE',  ( 0.000000000000000000, 0.000000000000000000, 1.000000000000000000 ) ) ;
#7344=( NAMED_UNIT ( * ) SI_UNIT ( $, .STERADIAN. ) SOLID_ANGLE_UNIT ( ) );
#7370=VERTEX_POINT ( 'NONE', #3857 ) ;
#7378=ORIENTED_EDGE ( 'NONE', *, *, #1773, .T. ) ;
#7385=VERTEX_POINT ( 'NONE', #7708 ) ;
#7387=( CONVERSION_BASED_UNIT ( 'INCH', #5545 ) LENGTH_UNIT ( ) NAMED_UNIT ( #4951 ) );
#7391=CARTESIAN_POINT ( 'NONE',  ( 0.000000000000000000, -0.03125000000000000000, 0.6646281645421511231 ) ) ;
#7407=EDGE_LOOP ( 'NONE', ( #4063, #7310, #2569, #6880 ) ) ;
#7421=DIRECTION ( 'NONE',  ( 1.000000000000000000, 0.000000000000000000, -0.000000000000000000 ) ) ;
#7454=FACE_BOUND ( 'NONE', #7178, .T. ) ;
#7483=PRODUCT_DEFINITION_FORMATION_WITH_SPECIFIED_SOURCE ( 'ANY', '', #7672, .NOT_KNOWN. ) ;
#7484=VERTEX_POINT ( 'NONE', #6289 ) ;
#7486=PLANE ( 'NONE',  #6752 ) ;
#7538=PLANE ( 'NONE',  #4399 ) ;
#7559=APPLICATION_CONTEXT ( 'configuration controlled 3d designs of mechanical parts and assemblies' ) ;
#7582=CARTESIAN_POINT ( 'NONE',  ( 0.1250000000000000278, 0.03125000000000000000, 0.06250000000000000000 ) ) ;
#7583=EDGE_CURVE ( 'NONE', #3663, #4400, #1772, .T. ) ;
#7641=ADVANCED_FACE ( 'NONE', ( #7667 ), #1965, .T. ) ;
#7667=FACE_OUTER_BOUND ( 'NONE', #422, .T. ) ;
#7672=PRODUCT ( 'Cleco, Fastener, Center, Split', 'Cleco, Fastener, Center, Split', '', ( #496 ) ) ;
#7687=EDGE_CURVE ( 'NONE', #2759, #4400, #3862, .T. ) ;
#7705=CARTESIAN_POINT ( 'NONE',  ( 0.1250000000000000278, -0.03125000000000000000, 0.06250000000000000000 ) ) ;
#7708=CARTESIAN_POINT ( 'NONE',  ( 0.1250000000000000278, -0.03125000000000000000, 0.000000000000000000 ) ) ;
#7730=LINE ( 'NONE', #4621, #2927 ) ;
#7748=ORIENTED_EDGE ( 'NONE', *, *, #3040, .F. ) ;
#7809=CARTESIAN_POINT ( 'NONE',  ( 0.000000000000000000, -0.03125000000000000000, 0.2896281645421511231 ) ) ;
#7823=FACE_OUTER_BOUND ( 'NONE', #3796, .T. ) ;
#7834=DIRECTION ( 'NONE',  ( -6.975840231036812635E-15, -1.000000000000000000, 2.013666839457971600E-30 ) ) ;
#7839=ORIENTED_EDGE ( 'NONE', *, *, #6093, .T. ) ;
#7846=CARTESIAN_POINT ( 'NONE',  ( 0.1250000000000000278, -0.03125000000000000000, 0.000000000000000000 ) ) ;
#7890=DIRECTION ( 'NONE',  ( 0.2873478855663426645, -0.000000000000000000, -0.9578262852211522071 ) ) ;
#7907=AXIS2_PLACEMENT_3D ( 'NONE', #3563, #7211, #3612 ) ;
#7913=VECTOR ( 'NONE', #221, 39.37007874015748143 ) ;
#7936=FACE_OUTER_BOUND ( 'NONE', #145, .T. ) ;
#7953=SHAPE_REPRESENTATION_RELATIONSHIP ( 'NONE' , 'NONE' ,  #2774, #3853 ) ;
#7954=ORIENTED_EDGE ( 'NONE', *, *, #6683, .T. ) ;
#7967=ORIENTED_EDGE ( 'NONE', *, *, #4388, .F. ) ;
#7990=ORIENTED_EDGE ( 'NONE', *, *, #5350, .T. ) ;
#8010=FACE_OUTER_BOUND ( 'NONE', #3066, .T. ) ;
#8017=DIRECTION ( 'NONE',  ( 0.000000000000000000, -0.000000000000000000, 1.000000000000000000 ) ) ;
#8037=ORIENTED_EDGE ( 'NONE', *, *, #5634, .T. ) ;
#8049=DIRECTION ( 'NONE',  ( 0.000000000000000000, -1.000000000000000000, 0.000000000000000000 ) ) ;
#8050=LINE ( 'NONE', #444, #6632 ) ;
#8079=EDGE_CURVE ( 'NONE', #5927, #7385, #6449, .T. ) ;
#8080=UNCERTAINTY_MEASURE_WITH_UNIT (LENGTH_MEASURE( 1.000000000000000082E-05 ), #7387, 'distance_accuracy_value', 'NONE');
#8129=COLOUR_RGB('Light Gray', 0.08235294, 0.09019608, 0.10196078);
#8130=FILL_AREA_STYLE_COLOUR('',#8129);
#8131=FILL_AREA_STYLE('',(#8130));
#8132=SURFACE_STYLE_FILL_AREA(#8131);
#8133=SURFACE_SIDE_STYLE('',(#8132));
#8134=SURFACE_STYLE_USAGE(.BOTH.,#8133);
#8135=PRESENTATION_STYLE_ASSIGNMENT((#8134));
#8150=STYLED_ITEM('',(#8135),#3760);
#8151=MECHANICAL_DESIGN_GEOMETRIC_PRESENTATION_REPRESENTATION('',(#8150),#2122);
ENDSEC;
END-ISO-10303-21;
